ISO-10303-21;
HEADER;
FILE_DESCRIPTION (('STEP AP214'),
    '1' );
FILE_NAME ('Slider.step',
    '2026-10-06T13:23:30',
    ( '' ),
    ( '' ),
    'SwSTEP 2.0',
    'SolidWorks 2020',
    '' );
FILE_SCHEMA (( 'AUTOMOTIVE_DESIGN' ));
ENDSEC;

DATA;
#107=ORIENTED_EDGE ( 'NONE', *, *, #17048, .F. ) ;
#202=ORIENTED_EDGE ( 'NONE', *, *, #2694, .F. ) ;
#216=CARTESIAN_POINT ( 'NONE',  ( -4.499999999959999109, 34.00000000000000000, -153.0552959529999839 ) ) ;
#228=VECTOR ( 'NONE', #3998, 1000.000000000000000 ) ;
#267=CARTESIAN_POINT ( 'NONE',  ( -4.499999999949999996, 40.00000000000000000, -150.0552959529999839 ) ) ;
#288=AXIS2_PLACEMENT_3D ( 'NONE', #20395, #13474, #22534 ) ;
#300=LINE ( 'NONE', #16373, #22571 ) ;
#326=ORIENTED_EDGE ( 'NONE', *, *, #7122, .T. ) ;
#363=EDGE_CURVE ( 'NONE', #23049, #12941, #18964, .T. ) ;
#366=DIRECTION ( 'NONE',  ( 1.000000000000000000, 0.000000000000000000, -2.259525899719999991E-12 ) ) ;
#477=VERTEX_POINT ( 'NONE', #7171 ) ;
#534=LINE ( 'NONE', #4213, #23018 ) ;
#549=ORIENTED_EDGE ( 'NONE', *, *, #9148, .T. ) ;
#572=CYLINDRICAL_SURFACE ( 'NONE', #7900, 2.500000000000001776 ) ;
#591=EDGE_LOOP ( 'NONE', ( #2730, #14318, #830, #3927 ) ) ;
#609=ORIENTED_EDGE ( 'NONE', *, *, #18363, .F. ) ;
#634=VERTEX_POINT ( 'NONE', #9534 ) ;
#637=ORIENTED_EDGE ( 'NONE', *, *, #7410, .T. ) ;
#643=CARTESIAN_POINT ( 'NONE',  ( -2.499999999940000439, 42.50000000000000000, -144.0552959529999839 ) ) ;
#646=VECTOR ( 'NONE', #14333, 1000.000000000000000 ) ;
#652=CARTESIAN_POINT ( 'NONE',  ( -4.499999999939999995, 34.80604359529999670, -142.8567321060000097 ) ) ;
#670=DIRECTION ( 'NONE',  ( 0.000000000000000000, 1.000000000000000000, 0.000000000000000000 ) ) ;
#724=DIRECTION ( 'NONE',  ( 1.000000000000000000, 0.000000000000000000, -2.259525899719999991E-12 ) ) ;
#766=LINE ( 'NONE', #643, #16554 ) ;
#772=AXIS2_PLACEMENT_3D ( 'NONE', #23480, #10382, #3617 ) ;
#775=VECTOR ( 'NONE', #2814, 1000.000000000000000 ) ;
#830=ORIENTED_EDGE ( 'NONE', *, *, #17504, .T. ) ;
#898=CARTESIAN_POINT ( 'NONE',  ( -4.499999999929999994, 41.25000000000000000, -138.0552959530000123 ) ) ;
#940=FACE_OUTER_BOUND ( 'NONE', #11497, .T. ) ;
#1018=ORIENTED_EDGE ( 'NONE', *, *, #17842, .T. ) ;
#1041=CARTESIAN_POINT ( 'NONE',  ( -4.499999999939999995, 37.00000000000000000, -144.0552959529999839 ) ) ;
#1070=LINE ( 'NONE', #15577, #9079 ) ;
#1081=ORIENTED_EDGE ( 'NONE', *, *, #17981, .F. ) ;
#1161=DIRECTION ( 'NONE',  ( 1.000000000000000000, 0.000000000000000000, 0.000000000000000000 ) ) ;
#1231=EDGE_CURVE ( 'NONE', #9331, #22451, #7548, .T. ) ;
#1278=EDGE_CURVE ( 'NONE', #14591, #5107, #14936, .T. ) ;
#1358=ORIENTED_EDGE ( 'NONE', *, *, #1231, .T. ) ;
#1377=CARTESIAN_POINT ( 'NONE',  ( -3.499999999920000437, 40.00000000000000000, -135.0552959530000123 ) ) ;
#1459=CARTESIAN_POINT ( 'NONE',  ( -2.499999999920000437, 40.00000000000000000, -135.0552959530000123 ) ) ;
#1561=ADVANCED_FACE ( 'NONE', ( #23481 ), #16230, .T. ) ;
#1677=ORIENTED_EDGE ( 'NONE', *, *, #8212, .T. ) ;
#1746=DIRECTION ( 'NONE',  ( 0.000000000000000000, 6.069065783950000909E-29, -1.000000000000000000 ) ) ;
#1822=LINE ( 'NONE', #14771, #2195 ) ;
#1824=ORIENTED_EDGE ( 'NONE', *, *, #17504, .F. ) ;
#1843=ORIENTED_EDGE ( 'NONE', *, *, #22120, .T. ) ;
#1868=ORIENTED_EDGE ( 'NONE', *, *, #5451, .T. ) ;
#1896=PRODUCT ( 'Slider', 'Slider', '', ( #14101 ) ) ;
#1981=FILL_AREA_STYLE_COLOUR ( '', #20998 ) ;
#2010=CARTESIAN_POINT ( 'NONE',  ( -4.499999999959999109, 34.00000000000000000, -153.0552959529999839 ) ) ;
#2021=FACE_OUTER_BOUND ( 'NONE', #591, .T. ) ;
#2046=LINE ( 'NONE', #7831, #12595 ) ;
#2062=ORIENTED_EDGE ( 'NONE', *, *, #4013, .T. ) ;
#2100=DIRECTION ( 'NONE',  ( -2.257157423930000049E-12, 0.000000000000000000, -1.000000000000000000 ) ) ;
#2163=CARTESIAN_POINT ( 'NONE',  ( -4.499999999949999996, 31.50000000000000000, -150.0552959529999839 ) ) ;
#2195=VECTOR ( 'NONE', #14891, 1000.000000000000000 ) ;
#2220=EDGE_CURVE ( 'NONE', #7796, #10437, #12426, .T. ) ;
#2225=ORIENTED_EDGE ( 'NONE', *, *, #4013, .F. ) ;
#2243=CARTESIAN_POINT ( 'NONE',  ( -2.599999999940000084, 37.00000000000000000, -144.0552959529999839 ) ) ;
#2246=CARTESIAN_POINT ( 'NONE',  ( -4.499999999939999995, 39.19395640469999620, -145.2538597989999971 ) ) ;
#2258=CARTESIAN_POINT ( 'NONE',  ( -4.499999999939999995, 37.00000000000000000, -144.0552959529999839 ) ) ;
#2299=( NAMED_UNIT ( * ) PLANE_ANGLE_UNIT ( ) SI_UNIT ( $, .RADIAN. ) );
#2391=EDGE_CURVE ( 'NONE', #10437, #23049, #300, .T. ) ;
#2401=LINE ( 'NONE', #2511, #22001 ) ;
#2404=ORIENTED_EDGE ( 'NONE', *, *, #22120, .F. ) ;
#2453=DIRECTION ( 'NONE',  ( 2.257157423930000049E-12, 0.000000000000000000, 1.000000000000000000 ) ) ;
#2498=EDGE_LOOP ( 'NONE', ( #6112, #12899, #5310, #14689 ) ) ;
#2511=CARTESIAN_POINT ( 'NONE',  ( -3.499999999949999996, 40.00000000000000000, -150.0552959529999839 ) ) ;
#2559=VERTEX_POINT ( 'NONE', #652 ) ;
#2569=MECHANICAL_DESIGN_GEOMETRIC_PRESENTATION_REPRESENTATION('',(#19668),#23454);
#2694=EDGE_CURVE ( 'NONE', #13175, #11596, #10273, .T. ) ;
#2730=ORIENTED_EDGE ( 'NONE', *, *, #7098, .F. ) ;
#2749=EDGE_LOOP ( 'NONE', ( #13497, #10323 ) ) ;
#2801=PRODUCT_DEFINITION_FORMATION_WITH_SPECIFIED_SOURCE ( 'ANY', '', #1896, .NOT_KNOWN. ) ;
#2814=DIRECTION ( 'NONE',  ( 0.000000000000000000, 1.000000000000000000, 0.000000000000000000 ) ) ;
#2819=DIRECTION ( 'NONE',  ( 0.000000000000000000, 6.069065783950000909E-29, -1.000000000000000000 ) ) ;
#2836=CARTESIAN_POINT ( 'NONE',  ( -4.499999999929999994, 42.50000000000000000, -138.0552959530000123 ) ) ;
#2890=VECTOR ( 'NONE', #17226, 1000.000000000000000 ) ;
#2915=ORIENTED_EDGE ( 'NONE', *, *, #2220, .T. ) ;
#3027=LINE ( 'NONE', #3142, #3483 ) ;
#3056=DIRECTION ( 'NONE',  ( -2.257157423930000049E-12, 0.000000000000000000, -1.000000000000000000 ) ) ;
#3057=UNCERTAINTY_MEASURE_WITH_UNIT (LENGTH_MEASURE( 1.000000000000000082E-05 ), #7536, 'distance_accuracy_value', 'NONE');
#3130=CARTESIAN_POINT ( 'NONE',  ( -4.499999999959999109, 40.00000000000000000, -153.0552959529999839 ) ) ;
#3142=CARTESIAN_POINT ( 'NONE',  ( -4.499999999959999109, 37.00000000000000000, -153.0552959529999839 ) ) ;
#3168=LINE ( 'NONE', #13980, #18931 ) ;
#3300=ORIENTED_EDGE ( 'NONE', *, *, #14055, .T. ) ;
#3330=LINE ( 'NONE', #4881, #13501 ) ;
#3367=ORIENTED_EDGE ( 'NONE', *, *, #19262, .T. ) ;
#3483=VECTOR ( 'NONE', #670, 1000.000000000000000 ) ;
#3523=CARTESIAN_POINT ( 'NONE',  ( -2.499999999940000439, 39.19395640469999620, -145.2538597999999865 ) ) ;
#3617=DIRECTION ( 'NONE',  ( -1.000000000000000000, 0.000000000000000000, 2.257171095940000041E-12 ) ) ;
#3622=CARTESIAN_POINT ( 'NONE',  ( -2.499999999940000439, 37.00000000000000000, -144.0552959529999839 ) ) ;
#3633=( LENGTH_UNIT ( ) NAMED_UNIT ( * ) SI_UNIT ( .MILLI., .METRE. ) );
#3728=SHAPE_REPRESENTATION ( 'Slider', ( #5025 ), #19488 ) ;
#3839=CARTESIAN_POINT ( 'NONE',  ( -4.499999999949999996, 34.00000000000000000, -150.0552959529999839 ) ) ;
#3871=( NAMED_UNIT ( * ) PLANE_ANGLE_UNIT ( ) SI_UNIT ( $, .RADIAN. ) );
#3880=ADVANCED_FACE ( 'NONE', ( #4022 ), #572, .F. ) ;
#3898=DIRECTION ( 'NONE',  ( 1.000000000000000000, 2.688820921349999492E-17, 0.000000000000000000 ) ) ;
#3927=ORIENTED_EDGE ( 'NONE', *, *, #19204, .F. ) ;
#3983=ORIENTED_EDGE ( 'NONE', *, *, #9951, .F. ) ;
#3998=DIRECTION ( 'NONE',  ( 0.000000000000000000, -1.000000000000000000, 0.000000000000000000 ) ) ;
#4013=EDGE_CURVE ( 'NONE', #22451, #14749, #15545, .T. ) ;
#4022=FACE_OUTER_BOUND ( 'NONE', #6398, .T. ) ;
#4023=CARTESIAN_POINT ( 'NONE',  ( -2.499999999929999994, 31.50000000000000000, -138.0552959530000123 ) ) ;
#4165=ORIENTED_EDGE ( 'NONE', *, *, #2391, .F. ) ;
#4179=AXIS2_PLACEMENT_3D ( 'NONE', #7301, #12761, #7176 ) ;
#4213=CARTESIAN_POINT ( 'NONE',  ( -4.499999999959999109, 34.00000000000000000, -151.5552959529999839 ) ) ;
#4376=CARTESIAN_POINT ( 'NONE',  ( -2.499999999929999994, 32.75000000000000000, -138.0552959530000123 ) ) ;
#4455=ORIENTED_EDGE ( 'NONE', *, *, #15213, .F. ) ;
#4470=VERTEX_POINT ( 'NONE', #1459 ) ;
#4475=ORIENTED_EDGE ( 'NONE', *, *, #19049, .F. ) ;
#4482=EDGE_CURVE ( 'NONE', #5769, #14591, #6564, .T. ) ;
#4490=AXIS2_PLACEMENT_3D ( 'NONE', #2010, #20076, #3898 ) ;
#4531=AXIS2_PLACEMENT_3D ( 'NONE', #21614, #14230, #1746 ) ;
#4590=CARTESIAN_POINT ( 'NONE',  ( 0.000000000000000000, 0.000000000000000000, 0.000000000000000000 ) ) ;
#4617=DIRECTION ( 'NONE',  ( -2.257144641399999941E-12, 0.000000000000000000, -1.000000000000000000 ) ) ;
#4621=CARTESIAN_POINT ( 'NONE',  ( -3.499999999920000437, 34.00000000000000000, -135.0552959530000123 ) ) ;
#4655=DIRECTION ( 'NONE',  ( 0.000000000000000000, 6.069065783950000909E-29, -1.000000000000000000 ) ) ;
#4727=ADVANCED_FACE ( 'NONE', ( #11411 ), #18449, .T. ) ;
#4824=DIRECTION ( 'NONE',  ( 1.000000000000000000, 0.000000000000000000, -2.259525899719999991E-12 ) ) ;
#4854=CARTESIAN_POINT ( 'NONE',  ( -3.500000048370000005, 34.80604359529999670, -142.8567321060000097 ) ) ;
#4881=CARTESIAN_POINT ( 'NONE',  ( -2.499999999959999997, 37.00000000000000000, -153.0552959529999839 ) ) ;
#4919=VERTEX_POINT ( 'NONE', #22719 ) ;
#4943=LINE ( 'NONE', #10504, #5938 ) ;
#5004=CARTESIAN_POINT ( 'NONE',  ( -2.499999999940000439, 37.00000000000000000, -144.0552959529999839 ) ) ;
#5025=AXIS2_PLACEMENT_3D ( 'NONE', #4590, #17084, #1161 ) ;
#5107=VERTEX_POINT ( 'NONE', #22340 ) ;
#5108=DIRECTION ( 'NONE',  ( 1.000000000000000000, 2.688820921349999492E-17, 0.000000000000000000 ) ) ;
#5186=ORIENTED_EDGE ( 'NONE', *, *, #8212, .F. ) ;
#5294=ORIENTED_EDGE ( 'NONE', *, *, #9665, .T. ) ;
#5298=DIRECTION ( 'NONE',  ( -2.257157423930000049E-12, 0.000000000000000000, -1.000000000000000000 ) ) ;
#5310=ORIENTED_EDGE ( 'NONE', *, *, #19049, .T. ) ;
#5337=VECTOR ( 'NONE', #2453, 1000.000000000000000 ) ;
#5419=STYLED_ITEM ( 'NONE', ( #7198 ), #18583 ) ;
#5444=ORIENTED_EDGE ( 'NONE', *, *, #1278, .T. ) ;
#5451=EDGE_CURVE ( 'NONE', #14557, #9232, #18134, .T. ) ;
#5478=LINE ( 'NONE', #11274, #19388 ) ;
#5530=SURFACE_STYLE_FILL_AREA ( #19933 ) ;
#5592=EDGE_CURVE ( 'NONE', #4919, #20880, #5976, .T. ) ;
#5769=VERTEX_POINT ( 'NONE', #3130 ) ;
#5781=AXIS2_PLACEMENT_3D ( 'NONE', #19116, #15544, #2819 ) ;
#5802=CARTESIAN_POINT ( 'NONE',  ( -2.499999999959999997, 40.00000000000000000, -153.0552959529999839 ) ) ;
#5816=ORIENTED_EDGE ( 'NONE', *, *, #16653, .T. ) ;
#5848=PLANE ( 'NONE',  #8797 ) ;
#5938=VECTOR ( 'NONE', #4824, 1000.000000000000000 ) ;
#5976=LINE ( 'NONE', #6103, #11346 ) ;
#6040=AXIS2_PLACEMENT_3D ( 'NONE', #14127, #13886, #16148 ) ;
#6048=DIRECTION ( 'NONE',  ( 0.000000000000000000, -1.000000000000000000, 0.000000000000000000 ) ) ;
#6103=CARTESIAN_POINT ( 'NONE',  ( -3.499999999949999996, 31.50000000000000000, -150.0552959529999839 ) ) ;
#6112=ORIENTED_EDGE ( 'NONE', *, *, #9665, .F. ) ;
#6233=ORIENTED_EDGE ( 'NONE', *, *, #22414, .T. ) ;
#6254=ORIENTED_EDGE ( 'NONE', *, *, #13885, .T. ) ;
#6398=EDGE_LOOP ( 'NONE', ( #9857, #14908, #1018, #14258 ) ) ;
#6498=LINE ( 'NONE', #9810, #22816 ) ;
#6564=LINE ( 'NONE', #12265, #7534 ) ;
#6654=LINE ( 'NONE', #19272, #21479 ) ;
#6673=ORIENTED_EDGE ( 'NONE', *, *, #16917, .T. ) ;
#6675=LINE ( 'NONE', #13937, #15303 ) ;
#6861=CYLINDRICAL_SURFACE ( 'NONE', #6040, 2.500000000000001776 ) ;
#6906=VECTOR ( 'NONE', #5298, 1000.000000000000000 ) ;
#7061=AXIS2_PLACEMENT_3D ( 'NONE', #15713, #12014, #19278 ) ;
#7098=EDGE_CURVE ( 'NONE', #7777, #634, #1822, .T. ) ;
#7122=EDGE_CURVE ( 'NONE', #10437, #15057, #7281, .T. ) ;
#7171=CARTESIAN_POINT ( 'NONE',  ( -2.499999999959999997, 34.00000000000000000, -153.0552959529999839 ) ) ;
#7174=ORIENTED_EDGE ( 'NONE', *, *, #12402, .F. ) ;
#7176=DIRECTION ( 'NONE',  ( 1.000000000000000000, 0.000000000000000000, -2.257171095940000041E-12 ) ) ;
#7183=CARTESIAN_POINT ( 'NONE',  ( -3.500000048370000005, 39.19395640469999620, -145.2538597999999865 ) ) ;
#7184=DIRECTION ( 'NONE',  ( 1.000000000000000000, -5.094701941669999797E-24, -2.257144641399999941E-12 ) ) ;
#7190=CARTESIAN_POINT ( 'NONE',  ( -2.499999999959999997, 34.00000000000000000, -151.5552959529999839 ) ) ;
#7198=PRESENTATION_STYLE_ASSIGNMENT (( #12666 ) ) ;
#7204=CARTESIAN_POINT ( 'NONE',  ( -2.499999999920000437, 34.00000000000000000, -135.0552959530000123 ) ) ;
#7240=ORIENTED_EDGE ( 'NONE', *, *, #13612, .T. ) ;
#7276=VERTEX_POINT ( 'NONE', #20601 ) ;
#7281=LINE ( 'NONE', #14550, #18910 ) ;
#7301=CARTESIAN_POINT ( 'NONE',  ( -4.499999999919999105, 40.00000000000000000, -135.0552959530000123 ) ) ;
#7358=ADVANCED_FACE ( 'NONE', ( #8050, #20800 ), #15435, .F. ) ;
#7410=EDGE_CURVE ( 'NONE', #11085, #20880, #11976, .T. ) ;
#7534=VECTOR ( 'NONE', #17393, 1000.000000000000000 ) ;
#7536=( LENGTH_UNIT ( ) NAMED_UNIT ( * ) SI_UNIT ( .MILLI., .METRE. ) );
#7537=VECTOR ( 'NONE', #22939, 1000.000000000000000 ) ;
#7548=LINE ( 'NONE', #20410, #19385 ) ;
#7777=VERTEX_POINT ( 'NONE', #3839 ) ;
#7792=FACE_OUTER_BOUND ( 'NONE', #14178, .T. ) ;
#7796=VERTEX_POINT ( 'NONE', #267 ) ;
#7831=CARTESIAN_POINT ( 'NONE',  ( -3.499999999929999994, 34.00000000000000000, -138.0552959530000123 ) ) ;
#7842=VECTOR ( 'NONE', #19212, 1000.000000000000000 ) ;
#7860=CARTESIAN_POINT ( 'NONE',  ( -4.499999999929999994, 42.50000000000000000, -138.0552959530000123 ) ) ;
#7900=AXIS2_PLACEMENT_3D ( 'NONE', #2243, #18653, #9467 ) ;
#7943=CARTESIAN_POINT ( 'NONE',  ( -2.499999999949999996, 31.50000000000000000, -150.0552959529999839 ) ) ;
#7958=DIRECTION ( 'NONE',  ( -1.000000000000000000, 0.000000000000000000, 2.257171095940000041E-12 ) ) ;
#7997=ADVANCED_FACE ( 'NONE', ( #9987 ), #17264, .F. ) ;
#7998=DIRECTION ( 'NONE',  ( 2.257157423930000049E-12, 0.000000000000000000, 1.000000000000000000 ) ) ;
#8050=FACE_BOUND ( 'NONE', #2749, .T. ) ;
#8122=DIRECTION ( 'NONE',  ( 0.000000000000000000, -1.000000000000000000, 0.000000000000000000 ) ) ;
#8212=EDGE_CURVE ( 'NONE', #14758, #9331, #5478, .T. ) ;
#8223=CARTESIAN_POINT ( 'NONE',  ( -4.499999999919999105, 40.00000000000000000, -135.0552959530000123 ) ) ;
#8268=VERTEX_POINT ( 'NONE', #10925 ) ;
#8321=DIRECTION ( 'NONE',  ( -2.257144641399999941E-12, 0.000000000000000000, -1.000000000000000000 ) ) ;
#8392=ORIENTED_EDGE ( 'NONE', *, *, #4482, .T. ) ;
#8395=LINE ( 'NONE', #22567, #775 ) ;
#8401=PLANE ( 'NONE',  #5781 ) ;
#8739=CARTESIAN_POINT ( 'NONE',  ( -4.499999999949999996, 41.25000000000000000, -150.0552959529999839 ) ) ;
#8797=AXIS2_PLACEMENT_3D ( 'NONE', #7860, #18819, #18934 ) ;
#8832=VECTOR ( 'NONE', #20501, 1000.000000000000000 ) ;
#8970=CARTESIAN_POINT ( 'NONE',  ( -4.499999999939999995, 31.50000000000000000, -144.0552959529999839 ) ) ;
#9079=VECTOR ( 'NONE', #14022, 1000.000000000000000 ) ;
#9081=SHAPE_REPRESENTATION_RELATIONSHIP ( 'NONE' , 'NONE' ,  #3728, #18583 ) ;
#9148=EDGE_CURVE ( 'NONE', #5769, #7796, #6498, .T. ) ;
#9181=EDGE_CURVE ( 'NONE', #4919, #7777, #8395, .T. ) ;
#9206=( NAMED_UNIT ( * ) PLANE_ANGLE_UNIT ( ) SI_UNIT ( $, .RADIAN. ) );
#9219=ORIENTED_EDGE ( 'NONE', *, *, #16917, .F. ) ;
#9232=VERTEX_POINT ( 'NONE', #3523 ) ;
#9243=PLANE ( 'NONE',  #14044 ) ;
#9331=VERTEX_POINT ( 'NONE', #16251 ) ;
#9351=ADVANCED_FACE ( 'NONE', ( #19477 ), #18150, .F. ) ;
#9467=DIRECTION ( 'NONE',  ( -1.082120504314331458E-12, 0.8775825618903714265, -0.4794255386042053368 ) ) ;
#9534=CARTESIAN_POINT ( 'NONE',  ( -2.499999999949999996, 34.00000000000000000, -150.0552959529999839 ) ) ;
#9644=ORIENTED_EDGE ( 'NONE', *, *, #15213, .T. ) ;
#9652=DIRECTION ( 'NONE',  ( 1.000000000000000000, 0.000000000000000000, -2.259525899719999991E-12 ) ) ;
#9665=EDGE_CURVE ( 'NONE', #12941, #11596, #16890, .T. ) ;
#9728=CARTESIAN_POINT ( 'NONE',  ( -4.499999999929999994, 40.00000000000000000, -138.0552959530000123 ) ) ;
#9810=CARTESIAN_POINT ( 'NONE',  ( -4.499999999959999109, 40.00000000000000000, -151.5552959529999839 ) ) ;
#9857=ORIENTED_EDGE ( 'NONE', *, *, #5451, .F. ) ;
#9951=EDGE_CURVE ( 'NONE', #20880, #634, #1070, .T. ) ;
#9987=FACE_OUTER_BOUND ( 'NONE', #15596, .T. ) ;
#10005=CARTESIAN_POINT ( 'NONE',  ( -4.499999999929999994, 31.50000000000000000, -138.0552959530000123 ) ) ;
#10031=ADVANCED_FACE ( 'NONE', ( #2021 ), #9243, .F. ) ;
#10066=DIRECTION ( 'NONE',  ( 2.257171095940000041E-12, -7.494005416210000121E-16, 1.000000000000000000 ) ) ;
#10255=EDGE_CURVE ( 'NONE', #2559, #14557, #22032, .T. ) ;
#10266=ORIENTED_EDGE ( 'NONE', *, *, #12192, .F. ) ;
#10273=LINE ( 'NONE', #17297, #12695 ) ;
#10323=ORIENTED_EDGE ( 'NONE', *, *, #10255, .T. ) ;
#10336=ORIENTED_EDGE ( 'NONE', *, *, #12192, .T. ) ;
#10382=DIRECTION ( 'NONE',  ( -2.257171095940000041E-12, 7.494005416210000121E-16, -1.000000000000000000 ) ) ;
#10437=VERTEX_POINT ( 'NONE', #20528 ) ;
#10502=SHAPE_DEFINITION_REPRESENTATION ( #21844, #3728 ) ;
#10504=CARTESIAN_POINT ( 'NONE',  ( -3.499999999929999994, 31.50000000000000000, -138.0552959530000123 ) ) ;
#10625=LINE ( 'NONE', #7190, #646 ) ;
#10640=EDGE_LOOP ( 'NONE', ( #1824, #17509, #8392, #12598 ) ) ;
#10684=PLANE ( 'NONE',  #21544 ) ;
#10793=ADVANCED_FACE ( 'NONE', ( #19452 ), #14443, .T. ) ;
#10795=FACE_OUTER_BOUND ( 'NONE', #17164, .T. ) ;
#10886=LINE ( 'NONE', #18166, #228 ) ;
#10891=LINE ( 'NONE', #22207, #12571 ) ;
#10900=CIRCLE ( 'NONE', #288, 2.500000000000002220 ) ;
#10925=CARTESIAN_POINT ( 'NONE',  ( -2.499999999929999994, 34.00000000000000000, -138.0552959530000123 ) ) ;
#10970=EDGE_LOOP ( 'NONE', ( #14883, #21545, #1868, #3367 ) ) ;
#11085=VERTEX_POINT ( 'NONE', #4023 ) ;
#11126=CARTESIAN_POINT ( 'NONE',  ( -4.499999999929999994, 34.00000000000000000, -138.0552959530000123 ) ) ;
#11236=PLANE ( 'NONE',  #4490 ) ;
#11274=CARTESIAN_POINT ( 'NONE',  ( -4.499999999919999105, 37.00000000000000000, -135.0552959530000123 ) ) ;
#11316=AXIS2_PLACEMENT_3D ( 'NONE', #2163, #11523, #7958 ) ;
#11346=VECTOR ( 'NONE', #9652, 1000.000000000000000 ) ;
#11367=ORIENTED_EDGE ( 'NONE', *, *, #5592, .T. ) ;
#11411=FACE_OUTER_BOUND ( 'NONE', #17742, .T. ) ;
#11421=FILL_AREA_STYLE ('',( #18703 ) ) ;
#11438=LINE ( 'NONE', #22170, #8832 ) ;
#11451=DIRECTION ( 'NONE',  ( -2.257157423930000049E-12, 0.000000000000000000, -1.000000000000000000 ) ) ;
#11497=EDGE_LOOP ( 'NONE', ( #13481, #11775, #5294, #202 ) ) ;
#11523=DIRECTION ( 'NONE',  ( -2.257171095940000041E-12, 7.494005416210000121E-16, -1.000000000000000000 ) ) ;
#11596=VERTEX_POINT ( 'NONE', #16571 ) ;
#11709=ORIENTED_EDGE ( 'NONE', *, *, #16396, .F. ) ;
#11775=ORIENTED_EDGE ( 'NONE', *, *, #363, .T. ) ;
#11950=PRODUCT_DEFINITION ( 'UNKNOWN', '', #2801, #23035 ) ;
#11976=LINE ( 'NONE', #16247, #22693 ) ;
#12014=DIRECTION ( 'NONE',  ( 1.000000000000000000, -5.094701941669999797E-24, -2.257144641399999941E-12 ) ) ;
#12045=ORIENTED_EDGE ( 'NONE', *, *, #9148, .F. ) ;
#12192=EDGE_CURVE ( 'NONE', #22451, #8268, #2046, .T. ) ;
#12249=DIRECTION ( 'NONE',  ( 1.000000000000000000, -5.094701941669999797E-24, -2.257144641399999941E-12 ) ) ;
#12265=CARTESIAN_POINT ( 'NONE',  ( -3.499999999959999997, 40.00000000000000000, -153.0552959529999839 ) ) ;
#12346=VERTEX_POINT ( 'NONE', #7204 ) ;
#12357=LINE ( 'NONE', #17851, #22652 ) ;
#12363=VECTOR ( 'NONE', #13896, 1000.000000000000000 ) ;
#12402=EDGE_CURVE ( 'NONE', #14749, #4919, #18492, .T. ) ;
#12426=LINE ( 'NONE', #8739, #15981 ) ;
#12501=ORIENTED_EDGE ( 'NONE', *, *, #22570, .F. ) ;
#12571=VECTOR ( 'NONE', #20419, 1000.000000000000000 ) ;
#12595=VECTOR ( 'NONE', #20581, 1000.000000000000000 ) ;
#12598=ORIENTED_EDGE ( 'NONE', *, *, #17365, .F. ) ;
#12612=VECTOR ( 'NONE', #8122, 1000.000000000000000 ) ;
#12666=SURFACE_STYLE_USAGE ( .BOTH. , #20290 ) ;
#12671=ADVANCED_FACE ( 'NONE', ( #16681 ), #5848, .T. ) ;
#12695=VECTOR ( 'NONE', #17539, 1000.000000000000000 ) ;
#12761=DIRECTION ( 'NONE',  ( 2.257171095940000041E-12, -7.494005416210000121E-16, 1.000000000000000000 ) ) ;
#12767=DIRECTION ( 'NONE',  ( 0.000000000000000000, 1.000000000000000000, 0.000000000000000000 ) ) ;
#12899=ORIENTED_EDGE ( 'NONE', *, *, #16396, .T. ) ;
#12941=VERTEX_POINT ( 'NONE', #9728 ) ;
#13096=ORIENTED_EDGE ( 'NONE', *, *, #5592, .F. ) ;
#13175=VERTEX_POINT ( 'NONE', #21296 ) ;
#13297=DIRECTION ( 'NONE',  ( 1.000000000000000000, -5.094701941669999797E-24, -2.257144641399999941E-12 ) ) ;
#13470=ADVANCED_FACE ( 'NONE', ( #19356 ), #8401, .F. ) ;
#13474=DIRECTION ( 'NONE',  ( 1.000000000000000000, -5.094701941669999797E-24, -2.257144641399999941E-12 ) ) ;
#13481=ORIENTED_EDGE ( 'NONE', *, *, #22414, .F. ) ;
#13497=ORIENTED_EDGE ( 'NONE', *, *, #17535, .T. ) ;
#13501=VECTOR ( 'NONE', #13690, 1000.000000000000000 ) ;
#13612=EDGE_CURVE ( 'NONE', #5107, #15057, #11438, .T. ) ;
#13622=EDGE_LOOP ( 'NONE', ( #17322, #549, #3300, #20667 ) ) ;
#13633=ORIENTED_EDGE ( 'NONE', *, *, #16653, .F. ) ;
#13690=DIRECTION ( 'NONE',  ( 0.000000000000000000, 1.000000000000000000, 0.000000000000000000 ) ) ;
#13705=FACE_OUTER_BOUND ( 'NONE', #10640, .T. ) ;
#13786=LINE ( 'NONE', #4621, #2890 ) ;
#13819=ADVANCED_FACE ( 'NONE', ( #13705 ), #21329, .T. ) ;
#13876=DIRECTION ( 'NONE',  ( 0.000000000000000000, -1.000000000000000000, 0.000000000000000000 ) ) ;
#13885=EDGE_CURVE ( 'NONE', #11596, #4470, #6675, .T. ) ;
#13886=DIRECTION ( 'NONE',  ( -1.000000000000000000, 1.458293570536846221E-24, 2.257144641401985094E-12 ) ) ;
#13896=DIRECTION ( 'NONE',  ( 1.000000000000000000, 0.000000000000000000, -2.267228047249999995E-12 ) ) ;
#13921=AXIS2_PLACEMENT_3D ( 'NONE', #3622, #7184, #12767 ) ;
#13937=CARTESIAN_POINT ( 'NONE',  ( -2.499999999920000437, 40.00000000000000000, -136.5552959530000123 ) ) ;
#13956=COLOUR_RGB ( '', 0.66274510, 0.83137255, 0.94901961) ;
#13980=CARTESIAN_POINT ( 'NONE',  ( -2.499999999920000437, 34.00000000000000000, -136.5552959530000123 ) ) ;
#14019=VECTOR ( 'NONE', #14326, 1000.000000000000000 ) ;
#14022=DIRECTION ( 'NONE',  ( 0.000000000000000000, 1.000000000000000000, 0.000000000000000000 ) ) ;
#14042=FACE_BOUND ( 'NONE', #19860, .T. ) ;
#14044=AXIS2_PLACEMENT_3D ( 'NONE', #216, #19618, #16509 ) ;
#14055=EDGE_CURVE ( 'NONE', #7796, #5107, #2401, .T. ) ;
#14101=PRODUCT_CONTEXT ( 'NONE', #17233, 'mechanical' ) ;
#14127=CARTESIAN_POINT ( 'NONE',  ( -2.599999999940000084, 37.00000000000000000, -144.0552959529999839 ) ) ;
#14178=EDGE_LOOP ( 'NONE', ( #1081, #1358, #10336, #21062 ) ) ;
#14230=DIRECTION ( 'NONE',  ( 2.688820921349999492E-17, -1.000000000000000000, -6.069065783950000909E-29 ) ) ;
#14258=ORIENTED_EDGE ( 'NONE', *, *, #18363, .T. ) ;
#14281=CARTESIAN_POINT ( 'NONE',  ( -4.499999999929999994, 42.50000000000000000, -138.0552959530000123 ) ) ;
#14318=ORIENTED_EDGE ( 'NONE', *, *, #17048, .T. ) ;
#14326=DIRECTION ( 'NONE',  ( 1.000000000000000000, 0.000000000000000000, -2.267228047249999995E-12 ) ) ;
#14333=DIRECTION ( 'NONE',  ( -2.257157423930000049E-12, 0.000000000000000000, -1.000000000000000000 ) ) ;
#14402=ORIENTED_EDGE ( 'NONE', *, *, #20421, .T. ) ;
#14443=PLANE ( 'NONE',  #772 ) ;
#14463=UNCERTAINTY_MEASURE_WITH_UNIT (LENGTH_MEASURE( 1.000000000000000082E-05 ), #22385, 'distance_accuracy_value', 'NONE');
#14550=CARTESIAN_POINT ( 'NONE',  ( -3.499999999949999996, 42.50000000000000000, -150.0552959529999839 ) ) ;
#14557=VERTEX_POINT ( 'NONE', #2246 ) ;
#14591=VERTEX_POINT ( 'NONE', #5802 ) ;
#14689=ORIENTED_EDGE ( 'NONE', *, *, #13885, .F. ) ;
#14749=VERTEX_POINT ( 'NONE', #10005 ) ;
#14758=VERTEX_POINT ( 'NONE', #8223 ) ;
#14771=CARTESIAN_POINT ( 'NONE',  ( -3.499999999949999996, 34.00000000000000000, -150.0552959529999839 ) ) ;
#14883=ORIENTED_EDGE ( 'NONE', *, *, #17842, .F. ) ;
#14891=DIRECTION ( 'NONE',  ( 1.000000000000000000, 0.000000000000000000, -2.259525899719999991E-12 ) ) ;
#14908=ORIENTED_EDGE ( 'NONE', *, *, #10255, .F. ) ;
#14936=LINE ( 'NONE', #22306, #5337 ) ;
#15007=ADVANCED_FACE ( 'NONE', ( #21509 ), #6861, .F. ) ;
#15022=AXIS2_PLACEMENT_3D ( 'NONE', #5004, #12249, #8321 ) ;
#15057=VERTEX_POINT ( 'NONE', #21629 ) ;
#15120=SURFACE_STYLE_USAGE ( .BOTH. , #18809 ) ;
#15213=EDGE_CURVE ( 'NONE', #4470, #12346, #10886, .T. ) ;
#15254=CLOSED_SHELL ( 'NONE', ( #7358, #18707, #12671, #20218, #1561, #9351, #17984, #7997, #10793, #13470, #13819, #10031, #4727, #3880, #17463, #15007 ) ) ;
#15303=VECTOR ( 'NONE', #21210, 1000.000000000000000 ) ;
#15421=EDGE_LOOP ( 'NONE', ( #10266, #2062, #5816, #2404 ) ) ;
#15435=PLANE ( 'NONE',  #21962 ) ;
#15511=EDGE_LOOP ( 'NONE', ( #22440, #2915, #326, #20325 ) ) ;
#15544=DIRECTION ( 'NONE',  ( 2.688820921349999492E-17, -1.000000000000000000, -6.069065783950000909E-29 ) ) ;
#15545=LINE ( 'NONE', #20672, #7537 ) ;
#15552=AXIS2_PLACEMENT_3D ( 'NONE', #1041, #22572, #13876 ) ;
#15574=DIRECTION ( 'NONE',  ( 0.000000000000000000, 1.000000000000000000, 0.000000000000000000 ) ) ;
#15577=CARTESIAN_POINT ( 'NONE',  ( -2.499999999949999996, 32.75000000000000000, -150.0552959529999839 ) ) ;
#15596=EDGE_LOOP ( 'NONE', ( #15701, #15887, #6233, #9219 ) ) ;
#15701=ORIENTED_EDGE ( 'NONE', *, *, #7122, .F. ) ;
#15713=CARTESIAN_POINT ( 'NONE',  ( -4.499999999939999995, 37.00000000000000000, -144.0552959529999839 ) ) ;
#15729=DIRECTION ( 'NONE',  ( -2.257171095940000041E-12, 7.494005416210000121E-16, -1.000000000000000000 ) ) ;
#15830=ORIENTED_EDGE ( 'NONE', *, *, #7098, .T. ) ;
#15884=ORIENTED_EDGE ( 'NONE', *, *, #9181, .T. ) ;
#15887=ORIENTED_EDGE ( 'NONE', *, *, #2391, .T. ) ;
#15911=LINE ( 'NONE', #4854, #12363 ) ;
#15981=VECTOR ( 'NONE', #15574, 1000.000000000000000 ) ;
#15997=VECTOR ( 'NONE', #6048, 1000.000000000000000 ) ;
#16059=ORIENTED_EDGE ( 'NONE', *, *, #12402, .T. ) ;
#16148=DIRECTION ( 'NONE',  ( -1.082120504314331458E-12, 0.8775825618903714265, -0.4794255386042053368 ) ) ;
#16192=EDGE_LOOP ( 'NONE', ( #18499, #22242, #20772, #5444, #7240, #6673, #17255, #6254, #9644, #14402, #1843, #637 ) ) ;
#16230=PLANE ( 'NONE',  #4179 ) ;
#16247=CARTESIAN_POINT ( 'NONE',  ( -2.499999999940000439, 31.50000000000000000, -144.0552959529999839 ) ) ;
#16251=CARTESIAN_POINT ( 'NONE',  ( -4.499999999919999105, 34.00000000000000000, -135.0552959530000123 ) ) ;
#16373=CARTESIAN_POINT ( 'NONE',  ( -4.499999999939999995, 42.50000000000000000, -144.0552959529999839 ) ) ;
#16396=EDGE_CURVE ( 'NONE', #12941, #14758, #6654, .T. ) ;
#16509=DIRECTION ( 'NONE',  ( 1.000000000000000000, 2.688820921349999492E-17, 0.000000000000000000 ) ) ;
#16554=VECTOR ( 'NONE', #7998, 1000.000000000000000 ) ;
#16556=SURFACE_STYLE_FILL_AREA ( #11421 ) ;
#16571=CARTESIAN_POINT ( 'NONE',  ( -2.499999999929999994, 40.00000000000000000, -138.0552959530000123 ) ) ;
#16652=CARTESIAN_POINT ( 'NONE',  ( -3.499999999929999994, 40.00000000000000000, -138.0552959530000123 ) ) ;
#16653=EDGE_CURVE ( 'NONE', #14749, #11085, #4943, .T. ) ;
#16681=FACE_OUTER_BOUND ( 'NONE', #15421, .T. ) ;
#16890=LINE ( 'NONE', #16652, #18966 ) ;
#16917=EDGE_CURVE ( 'NONE', #15057, #13175, #766, .T. ) ;
#17048=EDGE_CURVE ( 'NONE', #7777, #19702, #534, .T. ) ;
#17084=DIRECTION ( 'NONE',  ( 0.000000000000000000, 0.000000000000000000, 1.000000000000000000 ) ) ;
#17142=CARTESIAN_POINT ( 'NONE',  ( -4.499999999959999109, 34.00000000000000000, -153.0552959529999839 ) ) ;
#17164=EDGE_LOOP ( 'NONE', ( #13633, #16059, #11367, #21705 ) ) ;
#17226=DIRECTION ( 'NONE',  ( 1.000000000000000000, 0.000000000000000000, -2.259525899719999991E-12 ) ) ;
#17233=APPLICATION_CONTEXT ( 'automotive_design' ) ;
#17255=ORIENTED_EDGE ( 'NONE', *, *, #2694, .T. ) ;
#17264=PLANE ( 'NONE',  #18927 ) ;
#17297=CARTESIAN_POINT ( 'NONE',  ( -2.499999999929999994, 41.25000000000000000, -138.0552959530000123 ) ) ;
#17322=ORIENTED_EDGE ( 'NONE', *, *, #4482, .F. ) ;
#17343=DIRECTION ( 'NONE',  ( 1.000000000000000000, 0.000000000000000000, -2.257171095940000041E-12 ) ) ;
#17365=EDGE_CURVE ( 'NONE', #477, #14591, #3330, .T. ) ;
#17393=DIRECTION ( 'NONE',  ( 1.000000000000000000, 0.000000000000000000, -2.259525899719999991E-12 ) ) ;
#17463=ADVANCED_FACE ( 'NONE', ( #14042, #19162 ), #22860, .T. ) ;
#17504=EDGE_CURVE ( 'NONE', #19702, #477, #12357, .T. ) ;
#17509=ORIENTED_EDGE ( 'NONE', *, *, #22570, .T. ) ;
#17535=EDGE_CURVE ( 'NONE', #14557, #2559, #19620, .T. ) ;
#17539=DIRECTION ( 'NONE',  ( 0.000000000000000000, -1.000000000000000000, 0.000000000000000000 ) ) ;
#17583=MECHANICAL_DESIGN_GEOMETRIC_PRESENTATION_REPRESENTATION('',(#5419),#20253);
#17742=EDGE_LOOP ( 'NONE', ( #13096, #15884, #15830, #3983 ) ) ;
#17842=EDGE_CURVE ( 'NONE', #2559, #7276, #15911, .T. ) ;
#17851=CARTESIAN_POINT ( 'NONE',  ( -3.499999999959999997, 34.00000000000000000, -153.0552959529999839 ) ) ;
#17981=EDGE_CURVE ( 'NONE', #9331, #12346, #13786, .T. ) ;
#17984=ADVANCED_FACE ( 'NONE', ( #940 ), #19134, .T. ) ;
#18079=CARTESIAN_POINT ( 'NONE',  ( -4.499999999949999996, 31.50000000000000000, -150.0552959529999839 ) ) ;
#18088=DIRECTION ( 'NONE',  ( 0.000000000000000000, -1.000000000000000000, 0.000000000000000000 ) ) ;
#18134=LINE ( 'NONE', #7183, #14019 ) ;
#18150=PLANE ( 'NONE',  #4531 ) ;
#18166=CARTESIAN_POINT ( 'NONE',  ( -2.499999999920000437, 37.00000000000000000, -135.0552959530000123 ) ) ;
#18354=( NAMED_UNIT ( * ) SI_UNIT ( $, .STERADIAN. ) SOLID_ANGLE_UNIT ( ) );
#18363=EDGE_CURVE ( 'NONE', #7276, #9232, #18472, .T. ) ;
#18386=DIRECTION ( 'NONE',  ( 2.257157423930000049E-12, 0.000000000000000000, 1.000000000000000000 ) ) ;
#18426=EDGE_LOOP ( 'NONE', ( #4475, #1677, #22375, #4455 ) ) ;
#18449=PLANE ( 'NONE',  #11316 ) ;
#18472=CIRCLE ( 'NONE', #13921, 2.500000000000002220 ) ;
#18492=LINE ( 'NONE', #8970, #6906 ) ;
#18499=ORIENTED_EDGE ( 'NONE', *, *, #9951, .T. ) ;
#18583=ADVANCED_BREP_SHAPE_REPRESENTATION ( '', ( #19475, #5025 ), #19488 ) ;
#18614=( NAMED_UNIT ( * ) SI_UNIT ( $, .STERADIAN. ) SOLID_ANGLE_UNIT ( ) );
#18653=DIRECTION ( 'NONE',  ( -1.000000000000000000, 1.458293570536846221E-24, 2.257144641401985094E-12 ) ) ;
#18703=FILL_AREA_STYLE_COLOUR ( '', #13956 ) ;
#18707=ADVANCED_FACE ( 'NONE', ( #10795 ), #10684, .F. ) ;
#18809=SURFACE_SIDE_STYLE ('',( #16556 ) ) ;
#18819=DIRECTION ( 'NONE',  ( 2.257171095940000041E-12, -7.494005416210000121E-16, 1.000000000000000000 ) ) ;
#18910=VECTOR ( 'NONE', #21814, 1000.000000000000000 ) ;
#18927=AXIS2_PLACEMENT_3D ( 'NONE', #22732, #20964, #4655 ) ;
#18931=VECTOR ( 'NONE', #3056, 1000.000000000000000 ) ;
#18934=DIRECTION ( 'NONE',  ( 1.000000000000000000, 0.000000000000000000, -2.257171095940000041E-12 ) ) ;
#18964=LINE ( 'NONE', #898, #12612 ) ;
#18966=VECTOR ( 'NONE', #366, 1000.000000000000000 ) ;
#19049=EDGE_CURVE ( 'NONE', #14758, #4470, #22792, .T. ) ;
#19116=CARTESIAN_POINT ( 'NONE',  ( -4.499999999949999996, 40.00000000000000000, -150.0552959529999839 ) ) ;
#19120=ORIENTED_EDGE ( 'NONE', *, *, #1231, .F. ) ;
#19134=PLANE ( 'NONE',  #21510 ) ;
#19162=FACE_OUTER_BOUND ( 'NONE', #16192, .T. ) ;
#19176=CARTESIAN_POINT ( 'NONE',  ( -4.499999999959999109, 34.00000000000000000, -153.0552959529999839 ) ) ;
#19204=EDGE_CURVE ( 'NONE', #634, #477, #10625, .T. ) ;
#19210=APPLICATION_CONTEXT ( 'automotive_design' ) ;
#19212=DIRECTION ( 'NONE',  ( 1.000000000000000000, 0.000000000000000000, -2.259525899719999991E-12 ) ) ;
#19262=EDGE_CURVE ( 'NONE', #9232, #7276, #10900, .T. ) ;
#19272=CARTESIAN_POINT ( 'NONE',  ( -4.499999999919999105, 40.00000000000000000, -136.5552959530000123 ) ) ;
#19278=DIRECTION ( 'NONE',  ( 0.000000000000000000, -1.000000000000000000, 0.000000000000000000 ) ) ;
#19356=FACE_OUTER_BOUND ( 'NONE', #13622, .T. ) ;
#19385=VECTOR ( 'NONE', #2100, 1000.000000000000000 ) ;
#19388=VECTOR ( 'NONE', #18088, 1000.000000000000000 ) ;
#19452=FACE_OUTER_BOUND ( 'NONE', #15511, .T. ) ;
#19475=MANIFOLD_SOLID_BREP ( 'lock_assembly.1\\Product1.1\\Part2.1\\PartBody', #15254 ) ;
#19477=FACE_OUTER_BOUND ( 'NONE', #2498, .T. ) ;
#19488=( GEOMETRIC_REPRESENTATION_CONTEXT ( 3 ) GLOBAL_UNCERTAINTY_ASSIGNED_CONTEXT ( ( #3057 ) ) GLOBAL_UNIT_ASSIGNED_CONTEXT ( ( #7536, #3871, #21732 ) ) REPRESENTATION_CONTEXT ( 'NONE', 'WORKASPACE' ) );
#19525=DIRECTION ( 'NONE',  ( 1.000000000000000000, 0.000000000000000000, -2.259525899719999991E-12 ) ) ;
#19618=DIRECTION ( 'NONE',  ( -2.688820921349999492E-17, 1.000000000000000000, 6.069065783950000909E-29 ) ) ;
#19620=CIRCLE ( 'NONE', #7061, 2.500000000000002220 ) ;
#19668=STYLED_ITEM ( 'NONE', ( #20604 ), #19475 ) ;
#19702=VERTEX_POINT ( 'NONE', #17142 ) ;
#19819=DIRECTION ( 'NONE',  ( -2.257157423930000049E-12, 0.000000000000000000, -1.000000000000000000 ) ) ;
#19860=EDGE_LOOP ( 'NONE', ( #609, #23520 ) ) ;
#19933=FILL_AREA_STYLE ('',( #1981 ) ) ;
#20076=DIRECTION ( 'NONE',  ( -2.688820921349999492E-17, 1.000000000000000000, 6.069065783950000909E-29 ) ) ;
#20218=ADVANCED_FACE ( 'NONE', ( #7792 ), #11236, .F. ) ;
#20253=( GEOMETRIC_REPRESENTATION_CONTEXT ( 3 ) GLOBAL_UNCERTAINTY_ASSIGNED_CONTEXT ( ( #21607 ) ) GLOBAL_UNIT_ASSIGNED_CONTEXT ( ( #3633, #9206, #18614 ) ) REPRESENTATION_CONTEXT ( 'NONE', 'WORKASPACE' ) );
#20290=SURFACE_SIDE_STYLE ('',( #5530 ) ) ;
#20325=ORIENTED_EDGE ( 'NONE', *, *, #13612, .F. ) ;
#20395=CARTESIAN_POINT ( 'NONE',  ( -2.499999999940000439, 37.00000000000000000, -144.0552959529999839 ) ) ;
#20410=CARTESIAN_POINT ( 'NONE',  ( -4.499999999919999105, 34.00000000000000000, -136.5552959530000123 ) ) ;
#20419=DIRECTION ( 'NONE',  ( 1.000000000000000000, 0.000000000000000000, -2.259525899719999991E-12 ) ) ;
#20421=EDGE_CURVE ( 'NONE', #12346, #8268, #3168, .T. ) ;
#20501=DIRECTION ( 'NONE',  ( 0.000000000000000000, 1.000000000000000000, 0.000000000000000000 ) ) ;
#20528=CARTESIAN_POINT ( 'NONE',  ( -4.499999999949999996, 42.50000000000000000, -150.0552959529999839 ) ) ;
#20581=DIRECTION ( 'NONE',  ( 1.000000000000000000, 0.000000000000000000, -2.259525899719999991E-12 ) ) ;
#20601=CARTESIAN_POINT ( 'NONE',  ( -2.499999999940000439, 34.80604359529999670, -142.8567321060000097 ) ) ;
#20604=PRESENTATION_STYLE_ASSIGNMENT (( #15120 ) ) ;
#20667=ORIENTED_EDGE ( 'NONE', *, *, #1278, .F. ) ;
#20672=CARTESIAN_POINT ( 'NONE',  ( -4.499999999929999994, 32.75000000000000000, -138.0552959530000123 ) ) ;
#20772=ORIENTED_EDGE ( 'NONE', *, *, #17365, .T. ) ;
#20800=FACE_OUTER_BOUND ( 'NONE', #22319, .T. ) ;
#20880=VERTEX_POINT ( 'NONE', #7943 ) ;
#20956=DIRECTION ( 'NONE',  ( 2.257157423930000049E-12, 0.000000000000000000, 1.000000000000000000 ) ) ;
#20964=DIRECTION ( 'NONE',  ( 2.688820921349999492E-17, -1.000000000000000000, -6.069065783950000909E-29 ) ) ;
#20998=COLOUR_RGB ( '', 0.66274510, 0.83137255, 0.94901961) ;
#21014=AXIS2_PLACEMENT_3D ( 'NONE', #19176, #15729, #23225 ) ;
#21025=DIRECTION ( 'NONE',  ( 2.257157423930000049E-12, 0.000000000000000000, 1.000000000000000000 ) ) ;
#21062=ORIENTED_EDGE ( 'NONE', *, *, #20421, .F. ) ;
#21210=DIRECTION ( 'NONE',  ( 2.257157423930000049E-12, 0.000000000000000000, 1.000000000000000000 ) ) ;
#21296=CARTESIAN_POINT ( 'NONE',  ( -2.499999999929999994, 42.50000000000000000, -138.0552959530000123 ) ) ;
#21329=PLANE ( 'NONE',  #21014 ) ;
#21422=DIRECTION ( 'NONE',  ( -2.688820921349999492E-17, 1.000000000000000000, 6.069065783950000909E-29 ) ) ;
#21479=VECTOR ( 'NONE', #20956, 1000.000000000000000 ) ;
#21509=FACE_OUTER_BOUND ( 'NONE', #10970, .T. ) ;
#21510=AXIS2_PLACEMENT_3D ( 'NONE', #2836, #10066, #17343 ) ;
#21544=AXIS2_PLACEMENT_3D ( 'NONE', #18079, #21422, #5108 ) ;
#21545=ORIENTED_EDGE ( 'NONE', *, *, #17535, .F. ) ;
#21607=UNCERTAINTY_MEASURE_WITH_UNIT (LENGTH_MEASURE( 1.000000000000000082E-05 ), #3633, 'distance_accuracy_value', 'NONE');
#21614=CARTESIAN_POINT ( 'NONE',  ( -4.499999999949999996, 40.00000000000000000, -150.0552959529999839 ) ) ;
#21629=CARTESIAN_POINT ( 'NONE',  ( -2.499999999949999996, 42.50000000000000000, -150.0552959529999839 ) ) ;
#21705=ORIENTED_EDGE ( 'NONE', *, *, #7410, .F. ) ;
#21732=( NAMED_UNIT ( * ) SI_UNIT ( $, .STERADIAN. ) SOLID_ANGLE_UNIT ( ) );
#21814=DIRECTION ( 'NONE',  ( 1.000000000000000000, 0.000000000000000000, -2.259525899719999991E-12 ) ) ;
#21844=PRODUCT_DEFINITION_SHAPE ( 'NONE', 'NONE',  #11950 ) ;
#21962=AXIS2_PLACEMENT_3D ( 'NONE', #2258, #13297, #4617 ) ;
#22001=VECTOR ( 'NONE', #724, 1000.000000000000000 ) ;
#22032=CIRCLE ( 'NONE', #15552, 2.500000000000002220 ) ;
#22120=EDGE_CURVE ( 'NONE', #8268, #11085, #22351, .T. ) ;
#22170=CARTESIAN_POINT ( 'NONE',  ( -2.499999999949999996, 41.25000000000000000, -150.0552959529999839 ) ) ;
#22207=CARTESIAN_POINT ( 'NONE',  ( -3.499999999929999994, 42.50000000000000000, -138.0552959530000123 ) ) ;
#22242=ORIENTED_EDGE ( 'NONE', *, *, #19204, .T. ) ;
#22260=ORIENTED_EDGE ( 'NONE', *, *, #363, .F. ) ;
#22306=CARTESIAN_POINT ( 'NONE',  ( -2.499999999959999997, 40.00000000000000000, -151.5552959529999839 ) ) ;
#22319=EDGE_LOOP ( 'NONE', ( #7174, #2225, #19120, #5186, #11709, #22260, #4165, #22674, #12045, #12501, #107, #23000 ) ) ;
#22340=CARTESIAN_POINT ( 'NONE',  ( -2.499999999949999996, 40.00000000000000000, -150.0552959529999839 ) ) ;
#22351=LINE ( 'NONE', #4376, #15997 ) ;
#22375=ORIENTED_EDGE ( 'NONE', *, *, #17981, .T. ) ;
#22385=( LENGTH_UNIT ( ) NAMED_UNIT ( * ) SI_UNIT ( .MILLI., .METRE. ) );
#22414=EDGE_CURVE ( 'NONE', #23049, #13175, #10891, .T. ) ;
#22440=ORIENTED_EDGE ( 'NONE', *, *, #14055, .F. ) ;
#22451=VERTEX_POINT ( 'NONE', #11126 ) ;
#22534=DIRECTION ( 'NONE',  ( 0.000000000000000000, -1.000000000000000000, 0.000000000000000000 ) ) ;
#22567=CARTESIAN_POINT ( 'NONE',  ( -4.499999999949999996, 32.75000000000000000, -150.0552959529999839 ) ) ;
#22570=EDGE_CURVE ( 'NONE', #19702, #5769, #3027, .T. ) ;
#22571=VECTOR ( 'NONE', #18386, 1000.000000000000000 ) ;
#22572=DIRECTION ( 'NONE',  ( 1.000000000000000000, -5.094701941669999797E-24, -2.257144641399999941E-12 ) ) ;
#22652=VECTOR ( 'NONE', #19525, 1000.000000000000000 ) ;
#22674=ORIENTED_EDGE ( 'NONE', *, *, #2220, .F. ) ;
#22693=VECTOR ( 'NONE', #19819, 1000.000000000000000 ) ;
#22719=CARTESIAN_POINT ( 'NONE',  ( -4.499999999949999996, 31.50000000000000000, -150.0552959529999839 ) ) ;
#22732=CARTESIAN_POINT ( 'NONE',  ( -4.499999999929999994, 42.50000000000000000, -138.0552959530000123 ) ) ;
#22792=LINE ( 'NONE', #1377, #7842 ) ;
#22816=VECTOR ( 'NONE', #21025, 1000.000000000000000 ) ;
#22860=PLANE ( 'NONE',  #15022 ) ;
#22939=DIRECTION ( 'NONE',  ( 0.000000000000000000, -1.000000000000000000, 0.000000000000000000 ) ) ;
#23000=ORIENTED_EDGE ( 'NONE', *, *, #9181, .F. ) ;
#23018=VECTOR ( 'NONE', #11451, 1000.000000000000000 ) ;
#23035=PRODUCT_DEFINITION_CONTEXT ( 'detailed design', #19210, 'design' ) ;
#23049=VERTEX_POINT ( 'NONE', #14281 ) ;
#23225=DIRECTION ( 'NONE',  ( -1.000000000000000000, 0.000000000000000000, 2.257171095940000041E-12 ) ) ;
#23454=( GEOMETRIC_REPRESENTATION_CONTEXT ( 3 ) GLOBAL_UNCERTAINTY_ASSIGNED_CONTEXT ( ( #14463 ) ) GLOBAL_UNIT_ASSIGNED_CONTEXT ( ( #22385, #2299, #18354 ) ) REPRESENTATION_CONTEXT ( 'NONE', 'WORKASPACE' ) );
#23480=CARTESIAN_POINT ( 'NONE',  ( -4.499999999949999996, 31.50000000000000000, -150.0552959529999839 ) ) ;
#23481=FACE_OUTER_BOUND ( 'NONE', #18426, .T. ) ;
#23520=ORIENTED_EDGE ( 'NONE', *, *, #19262, .F. ) ;
ENDSEC;
END-ISO-10303-21;
